ISO-10303-21;
HEADER;
FILE_DESCRIPTION (('STEP AP214'),
    '1' );
FILE_NAME ('socket head cap screw_iso_ISO 4762 M4 x 20 - 20N.step',
    '2026-10-08T14:09:18',
    ( '' ),
    ( '' ),
    'SwSTEP 2.0',
    'SolidWorks 2026',
    '' );
FILE_SCHEMA (( 'AUTOMOTIVE_DESIGN' ));
ENDSEC;

DATA;
#7=VERTEX_POINT ( 'NONE', #1885 ) ;
#12=VECTOR ( 'NONE', #1631, 1000.000000000000227 ) ;
#14=CIRCLE ( 'NONE', #4735, 1.535500000000000087 ) ;
#19=ADVANCED_FACE ( 'NONE', ( #264 ), #4482, .F. ) ;
#22=EDGE_LOOP ( 'NONE', ( #4472, #3909, #3003, #3741, #4316 ) ) ;
#24=CIRCLE ( 'NONE', #1949, 3.500000000000000000 ) ;
#28=CIRCLE ( 'NONE', #4350, 3.500000000000000000 ) ;
#33=DIRECTION ( 'NONE',  ( -0.000000000000000000, 1.000000000000000000, 1.224646799147353207E-16 ) ) ;
#37=EDGE_LOOP ( 'NONE', ( #3778, #2575, #3763, #206 ) ) ;
#74=CARTESIAN_POINT ( 'NONE',  ( 2.000000000000000000, 1.329782007511006281, 0.7677499999999990443 ) ) ;
#92=VECTOR ( 'NONE', #1190, 1000.000000000000000 ) ;
#99=EDGE_CURVE ( 'NONE', #4080, #934, #4271, .T. ) ;
#106=CARTESIAN_POINT ( 'NONE',  ( 2.000000000000000000, -1.773042676681340968, 2.059984127722458425E-15 ) ) ;
#110=DIRECTION ( 'NONE',  ( 0.000000000000000000, -0.4999999999999993339, 0.8660254037844389297 ) ) ;
#118=AXIS2_PLACEMENT_3D ( 'NONE', #3711, #1384, #2920 ) ;
#158=ADVANCED_FACE ( 'NONE', ( #4205 ), #2001, .F. ) ;
#163=CARTESIAN_POINT ( 'NONE',  ( 0.1999999999999987899, 0.000000000000000000, 0.000000000000000000 ) ) ;
#176=CIRCLE ( 'NONE', #732, 3.500000000000000000 ) ;
#188=CARTESIAN_POINT ( 'NONE',  ( 2.000000000000000000, 1.773042676681340968, -2.276824562219559311E-15 ) ) ;
#197=CARTESIAN_POINT ( 'NONE',  ( 24.00000000000000000, 0.000000000000000000, 0.000000000000000000 ) ) ;
#198=ORIENTED_EDGE ( 'NONE', *, *, #2205, .T. ) ;
#199=DIRECTION ( 'NONE',  ( -1.000000000000000000, -0.000000000000000000, -0.000000000000000000 ) ) ;
#204=( NAMED_UNIT ( * ) SI_UNIT ( $, .STERADIAN. ) SOLID_ANGLE_UNIT ( ) );
#206=ORIENTED_EDGE ( 'NONE', *, *, #3845, .T. ) ;
#209=CARTESIAN_POINT ( 'NONE',  ( 24.00000000000000000, 0.000000000000000000, 1.610000000000000098 ) ) ;
#218=CARTESIAN_POINT ( 'NONE',  ( 4.199999999999995737, 2.449293598294707893E-16, -2.000000000000000888 ) ) ;
#228=EDGE_CURVE ( 'NONE', #497, #1504, #3710, .T. ) ;
#233=EDGE_CURVE ( 'NONE', #7, #497, #1330, .T. ) ;
#237=DIRECTION ( 'NONE',  ( -1.000000000000000000, -0.000000000000000000, -0.000000000000000000 ) ) ;
#239=DIRECTION ( 'NONE',  ( 0.000000000000000000, 0.5000000000000009992, 0.8660254037844381525 ) ) ;
#247=CIRCLE ( 'NONE', #2817, 2.200000000000001066 ) ;
#249=CARTESIAN_POINT ( 'NONE',  ( 2.000000000000000000, 1.773042676681340968, -2.276824562219559311E-15 ) ) ;
#255=ORIENTED_EDGE ( 'NONE', *, *, #4921, .F. ) ;
#256=AXIS2_PLACEMENT_3D ( 'NONE', #2633, #1779, #4840 ) ;
#258=FACE_OUTER_BOUND ( 'NONE', #2794, .T. ) ;
#264=FACE_OUTER_BOUND ( 'NONE', #2383, .T. ) ;
#271=EDGE_CURVE ( 'NONE', #2827, #2641, #3245, .T. ) ;
#276=DIRECTION ( 'NONE',  ( 0.000000000000000000, -0.5000000000000008882, -0.8660254037844380415 ) ) ;
#280=ORIENTED_EDGE ( 'NONE', *, *, #692, .F. ) ;
#296=PLANE ( 'NONE',  #570 ) ;
#297=VERTEX_POINT ( 'NONE', #1741 ) ;
#311=DIRECTION ( 'NONE',  ( 0.000000000000000000, 0.000000000000000000, -1.000000000000000000 ) ) ;
#312=CARTESIAN_POINT ( 'NONE',  ( 4.000000000000003553, 4.286263797015736595E-16, -3.500000000000000000 ) ) ;
#313=VERTEX_POINT ( 'NONE', #4471 ) ;
#325=TOROIDAL_SURFACE ( 'NONE', #3441, 2.200000000000001066, 0.2000000000000000111 ) ;
#342=VECTOR ( 'NONE', #2797, 1000.000000000000000 ) ;
#358=PLANE ( 'NONE',  #2103 ) ;
#363=EDGE_LOOP ( 'NONE', ( #280, #2338, #1740, #3798 ) ) ;
#366=CARTESIAN_POINT ( 'NONE',  ( 0.000000000000000000, 0.000000000000000000, 3.299999999999999822 ) ) ;
#368=DIRECTION ( 'NONE',  ( -1.000000000000000000, -0.000000000000000000, -0.000000000000000000 ) ) ;
#373=LINE ( 'NONE', #1177, #566 ) ;
#383=CARTESIAN_POINT ( 'NONE',  ( 24.00000000000000000, 0.000000000000000000, 0.000000000000000000 ) ) ;
#391=DIRECTION ( 'NONE',  ( 0.000000000000000000, 0.000000000000000000, 1.000000000000000000 ) ) ;
#392=VERTEX_POINT ( 'NONE', #3773 ) ;
#401=DIRECTION ( 'NONE',  ( -1.000000000000000000, -0.000000000000000000, -0.000000000000000000 ) ) ;
#426=VECTOR ( 'NONE', #276, 1000.000000000000227 ) ;
#428=MECHANICAL_DESIGN_GEOMETRIC_PRESENTATION_REPRESENTATION('',(#3228),#980);
#433=AXIS2_PLACEMENT_3D ( 'NONE', #3834, #2370, #2015 ) ;
#435=ORIENTED_EDGE ( 'NONE', *, *, #3052, .T. ) ;
#438=PLANE ( 'NONE',  #1771 ) ;
#441=EDGE_LOOP ( 'NONE', ( #4562, #4641 ) ) ;
#446=DIRECTION ( 'NONE',  ( 0.000000000000000000, -0.5000000000000008882, -0.8660254037844380415 ) ) ;
#461=ORIENTED_EDGE ( 'NONE', *, *, #692, .T. ) ;
#463=EDGE_CURVE ( 'NONE', #519, #313, #373, .T. ) ;
#473=ORIENTED_EDGE ( 'NONE', *, *, #4769, .F. ) ;
#482=EDGE_LOOP ( 'NONE', ( #3289, #3577, #3645, #3311 ) ) ;
#488=LINE ( 'NONE', #3935, #3383 ) ;
#497=VERTEX_POINT ( 'NONE', #4679 ) ;
#513=EDGE_CURVE ( 'NONE', #4266, #3976, #2404, .T. ) ;
#519=VERTEX_POINT ( 'NONE', #3555 ) ;
#526=LINE ( 'NONE', #3569, #722 ) ;
#534=DIRECTION ( 'NONE',  ( -1.000000000000000000, -0.000000000000000000, -0.000000000000000000 ) ) ;
#539=CARTESIAN_POINT ( 'NONE',  ( 3.999999999999997335, 2.694222958124178486E-16, 2.200000000000001066 ) ) ;
#540=DIRECTION ( 'NONE',  ( 1.000000000000000000, 0.000000000000000000, 0.000000000000000000 ) ) ;
#549=ORIENTED_EDGE ( 'NONE', *, *, #463, .T. ) ;
#560=FACE_BOUND ( 'NONE', #4671, .T. ) ;
#566=VECTOR ( 'NONE', #4170, 1000.000000000000114 ) ;
#570=AXIS2_PLACEMENT_3D ( 'NONE', #1893, #4491, #1117 ) ;
#572=AXIS2_PLACEMENT_3D ( 'NONE', #2796, #33, #1986 ) ;
#587=DIRECTION ( 'NONE',  ( 0.000000000000000000, 0.000000000000000000, 1.000000000000000000 ) ) ;
#595=CARTESIAN_POINT ( 'NONE',  ( 2.000000000000000000, 0.000000000000000000, 0.000000000000000000 ) ) ;
#598=ADVANCED_FACE ( 'NONE', ( #4325 ), #325, .F. ) ;
#613=PRODUCT ( 'socket head cap screw_iso_ISO 4762 M4 x 20 - 20N', 'socket head cap screw_iso_ISO 4762 M4 x 20 - 20N', '', ( #3146 ) ) ;
#615=DIRECTION ( 'NONE',  ( 0.000000000000000000, 0.000000000000000000, 1.000000000000000000 ) ) ;
#619=DIRECTION ( 'NONE',  ( -1.000000000000000000, -0.000000000000000000, -0.000000000000000000 ) ) ;
#632=DIRECTION ( 'NONE',  ( 0.000000000000000000, 0.000000000000000000, 1.000000000000000000 ) ) ;
#638=DIRECTION ( 'NONE',  ( 0.000000000000000000, 0.000000000000000000, 1.000000000000000000 ) ) ;
#660=FACE_OUTER_BOUND ( 'NONE', #1788, .T. ) ;
#662=CARTESIAN_POINT ( 'NONE',  ( 4.000000000000003553, 0.000000000000000000, 0.000000000000000000 ) ) ;
#663=ORIENTED_EDGE ( 'NONE', *, *, #1176, .T. ) ;
#666=AXIS2_PLACEMENT_3D ( 'NONE', #4115, #686, #239 ) ;
#671=ORIENTED_EDGE ( 'NONE', *, *, #1694, .T. ) ;
#675=VERTEX_POINT ( 'NONE', #218 ) ;
#676=DIRECTION ( 'NONE',  ( -1.000000000000000000, -0.000000000000000000, -0.000000000000000000 ) ) ;
#679=ORIENTED_EDGE ( 'NONE', *, *, #1273, .F. ) ;
#680=ORIENTED_EDGE ( 'NONE', *, *, #2473, .T. ) ;
#686=DIRECTION ( 'NONE',  ( 0.000000000000000000, 0.8660254037844381525, -0.5000000000000009992 ) ) ;
#690=EDGE_CURVE ( 'NONE', #4023, #3361, #4322, .T. ) ;
#692=EDGE_CURVE ( 'NONE', #4023, #675, #2130, .T. ) ;
#702=ORIENTED_EDGE ( 'NONE', *, *, #3113, .T. ) ;
#703=CARTESIAN_POINT ( 'NONE',  ( 4.199999999999995737, 2.694222958124178486E-16, 2.200000000000001066 ) ) ;
#704=CARTESIAN_POINT ( 'NONE',  ( 2.000000000000000000, 1.773042676681340968, -2.276824562219559311E-15 ) ) ;
#709=EDGE_CURVE ( 'NONE', #297, #4462, #2906, .T. ) ;
#721=DIRECTION ( 'NONE',  ( 0.000000000000000000, 0.000000000000000000, 1.000000000000000000 ) ) ;
#722=VECTOR ( 'NONE', #786, 1000.000000000000000 ) ;
#726=ORIENTED_EDGE ( 'NONE', *, *, #4181, .T. ) ;
#727=AXIS2_PLACEMENT_3D ( 'NONE', #2613, #3752, #4129 ) ;
#732=AXIS2_PLACEMENT_3D ( 'NONE', #1683, #1380, #2536 ) ;
#734=AXIS2_PLACEMENT_3D ( 'NONE', #2871, #2065, #2419 ) ;
#739=AXIS2_PLACEMENT_3D ( 'NONE', #742, #763, #391 ) ;
#742=CARTESIAN_POINT ( 'NONE',  ( -31.74999999999995737, 0.000000000000000000, 0.000000000000000000 ) ) ;
#751=EDGE_CURVE ( 'NONE', #1504, #3948, #2245, .T. ) ;
#763=DIRECTION ( 'NONE',  ( -1.000000000000000000, -0.000000000000000000, -0.000000000000000000 ) ) ;
#776=EDGE_CURVE ( 'NONE', #313, #1525, #1394, .T. ) ;
#777=MECHANICAL_DESIGN_GEOMETRIC_PRESENTATION_REPRESENTATION('',(#4945),#4454);
#784=ADVANCED_FACE ( 'NONE', ( #4441 ), #2889, .F. ) ;
#786=DIRECTION ( 'NONE',  ( 0.000000000000000000, -1.000000000000000000, 9.783878858594330870E-16 ) ) ;
#799=DIRECTION ( 'NONE',  ( -0.7071067811865359154, 8.659560562355074607E-17, -0.7071067811865591191 ) ) ;
#805=DIRECTION ( 'NONE',  ( 1.000000000000000000, 0.000000000000000000, 0.000000000000000000 ) ) ;
#817=AXIS2_PLACEMENT_3D ( 'NONE', #383, #3437, #1166 ) ;
#828=EDGE_LOOP ( 'NONE', ( #2198, #680, #835, #671, #2741 ) ) ;
#835=ORIENTED_EDGE ( 'NONE', *, *, #3508, .T. ) ;
#838=CARTESIAN_POINT ( 'NONE',  ( -31.74999999999995737, 4.286263797015736595E-16, -3.500000000000000000 ) ) ;
#863=LINE ( 'NONE', #188, #4336 ) ;
#866=LINE ( 'NONE', #2374, #1925 ) ;
#893=DIRECTION ( 'NONE',  ( 0.000000000000000000, 0.000000000000000000, 1.000000000000000000 ) ) ;
#896=AXIS2_PLACEMENT_3D ( 'NONE', #1494, #676, #721 ) ;
#899=DIRECTION ( 'NONE',  ( 0.000000000000000000, 0.000000000000000000, -1.000000000000000000 ) ) ;
#902=CIRCLE ( 'NONE', #1617, 1.610000000000000098 ) ;
#904=ADVANCED_FACE ( 'NONE', ( #2625 ), #296, .F. ) ;
#922=DIRECTION ( 'NONE',  ( 0.000000000000000000, 1.000000000000000000, -1.467581828789149532E-15 ) ) ;
#925=DIRECTION ( 'NONE',  ( 0.000000000000000000, 0.000000000000000000, 1.000000000000000000 ) ) ;
#928=DIRECTION ( 'NONE',  ( 0.000000000000000000, 0.000000000000000000, 1.000000000000000000 ) ) ;
#934=VERTEX_POINT ( 'NONE', #2604 ) ;
#947=DIRECTION ( 'NONE',  ( -1.000000000000000000, -0.000000000000000000, -0.000000000000000000 ) ) ;
#956=FACE_OUTER_BOUND ( 'NONE', #441, .T. ) ;
#958=FACE_OUTER_BOUND ( 'NONE', #3956, .T. ) ;
#961=LINE ( 'NONE', #2493, #1519 ) ;
#979=AXIS2_PLACEMENT_3D ( 'NONE', #2447, #540, #3966 ) ;
#980=( GEOMETRIC_REPRESENTATION_CONTEXT ( 3 ) GLOBAL_UNCERTAINTY_ASSIGNED_CONTEXT ( ( #3402 ) ) GLOBAL_UNIT_ASSIGNED_CONTEXT ( ( #4707, #1310, #204 ) ) REPRESENTATION_CONTEXT ( 'NONE', 'WORKASPACE' ) );
#988=DIRECTION ( 'NONE',  ( -1.000000000000000000, -0.000000000000000000, -0.000000000000000000 ) ) ;
#990=FACE_OUTER_BOUND ( 'NONE', #3983, .T. ) ;
#1006=DIRECTION ( 'NONE',  ( 0.000000000000000000, 0.000000000000000000, 1.000000000000000000 ) ) ;
#1011=CARTESIAN_POINT ( 'NONE',  ( 24.00000000000000000, 2.210487472460972698E-16, -1.610000000000000098 ) ) ;
#1015=FACE_OUTER_BOUND ( 'NONE', #3253, .T. ) ;
#1033=TOROIDAL_SURFACE ( 'NONE', #1674, 2.200000000000001066, 0.2000000000000000111 ) ;
#1034=CARTESIAN_POINT ( 'NONE',  ( 24.00000000000000000, 0.000000000000000000, 0.000000000000000000 ) ) ;
#1048=CIRCLE ( 'NONE', #433, 0.2000000000000000944 ) ;
#1055=DIRECTION ( 'NONE',  ( 0.000000000000000000, 0.8660254037844380415, -0.5000000000000012212 ) ) ;
#1056=PLANE ( 'NONE',  #1304 ) ;
#1078=ORIENTED_EDGE ( 'NONE', *, *, #1155, .T. ) ;
#1080=CARTESIAN_POINT ( 'NONE',  ( 2.000000000000000000, 1.773042676681340968, -2.276824562219559311E-15 ) ) ;
#1091=ORIENTED_EDGE ( 'NONE', *, *, #1784, .T. ) ;
#1107=EDGE_CURVE ( 'NONE', #3361, #4685, #866, .T. ) ;
#1113=ORIENTED_EDGE ( 'NONE', *, *, #1249, .T. ) ;
#1115=DIRECTION ( 'NONE',  ( 1.000000000000000000, 0.000000000000000000, 0.000000000000000000 ) ) ;
#1117=DIRECTION ( 'NONE',  ( 0.000000000000000000, -1.000000000000000000, 1.467581828789149729E-15 ) ) ;
#1128=CYLINDRICAL_SURFACE ( 'NONE', #1851, 2.000000000000000888 ) ;
#1136=PRESENTATION_STYLE_ASSIGNMENT (( #3806 ) ) ;
#1137=CARTESIAN_POINT ( 'NONE',  ( 0.1999999999999987899, 0.000000000000000000, 0.000000000000000000 ) ) ;
#1140=CARTESIAN_POINT ( 'NONE',  ( 2.000000000000000000, -0.8865213383406690406, 1.535500000000000975 ) ) ;
#1146=CARTESIAN_POINT ( 'NONE',  ( 0.000000000000000000, 0.000000000000000000, 0.000000000000000000 ) ) ;
#1153=ORIENTED_EDGE ( 'NONE', *, *, #1637, .F. ) ;
#1154=EDGE_CURVE ( 'NONE', #675, #2827, #2893, .T. ) ;
#1155=EDGE_CURVE ( 'NONE', #1504, #1323, #526, .T. ) ;
#1166=DIRECTION ( 'NONE',  ( 0.000000000000000000, 0.000000000000000000, 1.000000000000000000 ) ) ;
#1176=EDGE_CURVE ( 'NONE', #4766, #1283, #3527, .T. ) ;
#1177=CARTESIAN_POINT ( 'NONE',  ( 0.000000000000000000, 1.773042676681340968, -2.276824562219559311E-15 ) ) ;
#1187=EDGE_CURVE ( 'NONE', #4462, #1525, #961, .T. ) ;
#1190=DIRECTION ( 'NONE',  ( -1.000000000000000000, -0.000000000000000000, -0.000000000000000000 ) ) ;
#1194=ORIENTED_EDGE ( 'NONE', *, *, #271, .T. ) ;
#1213=PLANE ( 'NONE',  #1216 ) ;
#1216=AXIS2_PLACEMENT_3D ( 'NONE', #2289, #805, #2369 ) ;
#1240=EDGE_CURVE ( 'NONE', #3948, #392, #3931, .T. ) ;
#1249=EDGE_CURVE ( 'NONE', #2708, #3361, #4014, .T. ) ;
#1251=LINE ( 'NONE', #2608, #4905 ) ;
#1253=FACE_OUTER_BOUND ( 'NONE', #3079, .T. ) ;
#1263=FACE_OUTER_BOUND ( 'NONE', #1825, .T. ) ;
#1265=CARTESIAN_POINT ( 'NONE',  ( 2.000000000000000000, 0.8865213383406717051, 1.535499999999998533 ) ) ;
#1270=DIRECTION ( 'NONE',  ( 0.000000000000000000, -1.000000000000000000, 0.000000000000000000 ) ) ;
#1272=ORIENTED_EDGE ( 'NONE', *, *, #233, .F. ) ;
#1273=EDGE_CURVE ( 'NONE', #1595, #4266, #1357, .T. ) ;
#1278=EDGE_CURVE ( 'NONE', #2641, #2827, #247, .T. ) ;
#1283=VERTEX_POINT ( 'NONE', #3291 ) ;
#1295=VECTOR ( 'NONE', #3176, 1000.000000000000000 ) ;
#1304=AXIS2_PLACEMENT_3D ( 'NONE', #4109, #3708, #4864 ) ;
#1310=( NAMED_UNIT ( * ) PLANE_ANGLE_UNIT ( ) SI_UNIT ( $, .RADIAN. ) );
#1314=AXIS2_PLACEMENT_3D ( 'NONE', #1789, #4511, #4090 ) ;
#1318=CARTESIAN_POINT ( 'NONE',  ( 2.000000000000000000, 1.773042676681340968, -2.276824562219559311E-15 ) ) ;
#1323=VERTEX_POINT ( 'NONE', #4434 ) ;
#1324=CARTESIAN_POINT ( 'NONE',  ( 2.000000000000000000, 0.8865213383406685965, -1.535500000000000753 ) ) ;
#1326=SHAPE_REPRESENTATION ( 'socket head cap screw_iso_ISO 4762 M4 x 20 - 20N', ( #1918 ), #2148 ) ;
#1327=VERTEX_POINT ( 'NONE', #1011 ) ;
#1330=LINE ( 'NONE', #249, #3792 ) ;
#1349=DIRECTION ( 'NONE',  ( -1.000000000000000000, -0.000000000000000000, -0.000000000000000000 ) ) ;
#1352=FACE_OUTER_BOUND ( 'NONE', #3474, .T. ) ;
#1353=ADVANCED_FACE ( 'NONE', ( #3340 ), #2737, .T. ) ;
#1356=( NAMED_UNIT ( * ) PLANE_ANGLE_UNIT ( ) SI_UNIT ( $, .RADIAN. ) );
#1357=LINE ( 'NONE', #4388, #2414 ) ;
#1363=ORIENTED_EDGE ( 'NONE', *, *, #1576, .T. ) ;
#1365=CARTESIAN_POINT ( 'NONE',  ( -31.74999999999995737, 2.449293598294707893E-16, -2.000000000000000888 ) ) ;
#1375=ORIENTED_EDGE ( 'NONE', *, *, #271, .F. ) ;
#1380=DIRECTION ( 'NONE',  ( -1.000000000000000000, -0.000000000000000000, -0.000000000000000000 ) ) ;
#1382=CARTESIAN_POINT ( 'NONE',  ( 2.000000000000000000, 2.253471898105738645E-15, 1.535499999999999865 ) ) ;
#1384=DIRECTION ( 'NONE',  ( 1.000000000000000000, 0.000000000000000000, 0.000000000000000000 ) ) ;
#1394=LINE ( 'NONE', #4757, #2168 ) ;
#1397=CARTESIAN_POINT ( 'NONE',  ( 0.000000000000000000, -1.773042676681340968, 2.059984127722458425E-15 ) ) ;
#1404=EDGE_LOOP ( 'NONE', ( #4681, #3073, #3892 ) ) ;
#1407=ADVANCED_BREP_SHAPE_REPRESENTATION ( '', ( #2009, #1918 ), #2148 ) ;
#1415=EDGE_CURVE ( 'NONE', #4685, #2641, #3296, .T. ) ;
#1428=DIRECTION ( 'NONE',  ( 0.000000000000000000, 0.000000000000000000, -1.000000000000000000 ) ) ;
#1440=FACE_OUTER_BOUND ( 'NONE', #363, .T. ) ;
#1460=FACE_OUTER_BOUND ( 'NONE', #4318, .T. ) ;
#1484=ADVANCED_FACE ( 'NONE', ( #2970 ), #3685, .T. ) ;
#1486=ORIENTED_EDGE ( 'NONE', *, *, #4172, .F. ) ;
#1491=CARTESIAN_POINT ( 'NONE',  ( 4.199999999999995737, 0.000000000000000000, 2.000000000000000888 ) ) ;
#1493=EDGE_LOOP ( 'NONE', ( #2466, #4792, #2319, #1627, #2622 ) ) ;
#1494=CARTESIAN_POINT ( 'NONE',  ( 2.000000000000000000, 0.000000000000000000, 0.000000000000000000 ) ) ;
#1504=VERTEX_POINT ( 'NONE', #2312 ) ;
#1517=ORIENTED_EDGE ( 'NONE', *, *, #1694, .F. ) ;
#1518=VERTEX_POINT ( 'NONE', #3121 ) ;
#1519=VECTOR ( 'NONE', #3227, 1000.000000000000227 ) ;
#1525=VERTEX_POINT ( 'NONE', #2340 ) ;
#1540=CARTESIAN_POINT ( 'NONE',  ( 4.199999999999995737, 0.000000000000000000, -2.200000000000001066 ) ) ;
#1543=EDGE_LOOP ( 'NONE', ( #4236, #4956, #2529, #1904, #4504, #4661 ) ) ;
#1545=ADVANCED_FACE ( 'NONE', ( #1263 ), #1213, .F. ) ;
#1546=CLOSED_SHELL ( 'NONE', ( #784, #1484, #598, #1353, #1952, #3210, #4290, #2047, #2783, #3681, #3811, #4121, #4790, #1721, #2788, #904, #3985, #1890, #4026, #2935, #19, #3384, #2384, #2449, #158, #1545, #1797 ) ) ;
#1547=VECTOR ( 'NONE', #446, 1000.000000000000227 ) ;
#1549=ORIENTED_EDGE ( 'NONE', *, *, #3297, .T. ) ;
#1552=VECTOR ( 'NONE', #1733, 1000.000000000000000 ) ;
#1553=AXIS2_PLACEMENT_3D ( 'NONE', #4048, #619, #4760 ) ;
#1564=ORIENTED_EDGE ( 'NONE', *, *, #99, .T. ) ;
#1570=ORIENTED_EDGE ( 'NONE', *, *, #1637, .T. ) ;
#1576=EDGE_CURVE ( 'NONE', #3989, #4766, #4262, .T. ) ;
#1579=ORIENTED_EDGE ( 'NONE', *, *, #233, .T. ) ;
#1595=VERTEX_POINT ( 'NONE', #3147 ) ;
#1600=AXIS2_PLACEMENT_3D ( 'NONE', #3644, #947, #928 ) ;
#1601=ORIENTED_EDGE ( 'NONE', *, *, #4523, .F. ) ;
#1602=EDGE_CURVE ( 'NONE', #519, #4198, #4312, .T. ) ;
#1615=VECTOR ( 'NONE', #4309, 1000.000000000000000 ) ;
#1617=AXIS2_PLACEMENT_3D ( 'NONE', #3584, #4430, #1006 ) ;
#1627=ORIENTED_EDGE ( 'NONE', *, *, #2803, .T. ) ;
#1629=FILL_AREA_STYLE_COLOUR ( '', #2582 ) ;
#1631=DIRECTION ( 'NONE',  ( 0.000000000000000000, 0.4999999999999990008, -0.8660254037844391517 ) ) ;
#1637=EDGE_CURVE ( 'NONE', #2708, #1327, #4332, .T. ) ;
#1674=AXIS2_PLACEMENT_3D ( 'NONE', #2784, #3621, #2030 ) ;
#1683=CARTESIAN_POINT ( 'NONE',  ( 4.000000000000003553, 0.000000000000000000, 0.000000000000000000 ) ) ;
#1684=PLANE ( 'NONE',  #979 ) ;
#1687=ORIENTED_EDGE ( 'NONE', *, *, #4298, .T. ) ;
#1692=DIRECTION ( 'NONE',  ( -1.000000000000000000, -0.000000000000000000, -0.000000000000000000 ) ) ;
#1694=EDGE_CURVE ( 'NONE', #3027, #497, #14, .T. ) ;
#1696=AXIS2_PLACEMENT_3D ( 'NONE', #4526, #1055, #2994 ) ;
#1717=CARTESIAN_POINT ( 'NONE',  ( 0.1999999999999987899, 4.286263797015736595E-16, -3.500000000000000000 ) ) ;
#1720=DIRECTION ( 'NONE',  ( 0.000000000000000000, 0.000000000000000000, -1.000000000000000000 ) ) ;
#1721=ADVANCED_FACE ( 'NONE', ( #3283 ), #3453, .T. ) ;
#1732=( LENGTH_UNIT ( ) NAMED_UNIT ( * ) SI_UNIT ( .MILLI., .METRE. ) );
#1733=DIRECTION ( 'NONE',  ( -0.7071067811865359154, 0.000000000000000000, 0.7071067811865591191 ) ) ;
#1740=ORIENTED_EDGE ( 'NONE', *, *, #1107, .T. ) ;
#1741=CARTESIAN_POINT ( 'NONE',  ( 0.000000000000000000, -0.8865213383406690406, 1.535500000000000975 ) ) ;
#1758=EDGE_CURVE ( 'NONE', #3948, #1323, #4813, .T. ) ;
#1765=AXIS2_PLACEMENT_3D ( 'NONE', #4794, #237, #587 ) ;
#1770=DIRECTION ( 'NONE',  ( -1.000000000000000000, -0.000000000000000000, -0.000000000000000000 ) ) ;
#1771=AXIS2_PLACEMENT_3D ( 'NONE', #1080, #4914, #3476 ) ;
#1778=DIRECTION ( 'NONE',  ( 0.000000000000000000, -0.4999999999999990563, 0.8660254037844391517 ) ) ;
#1779=DIRECTION ( 'NONE',  ( 1.000000000000000000, 0.000000000000000000, 0.000000000000000000 ) ) ;
#1784=EDGE_CURVE ( 'NONE', #1327, #2708, #902, .T. ) ;
#1788=EDGE_LOOP ( 'NONE', ( #4680, #2042, #2561 ) ) ;
#1789=CARTESIAN_POINT ( 'NONE',  ( 2.000000000000000000, 0.8865213383406685965, -1.535500000000000753 ) ) ;
#1792=ORIENTED_EDGE ( 'NONE', *, *, #1415, .T. ) ;
#1793=CARTESIAN_POINT ( 'NONE',  ( 23.61000000000001364, 0.000000000000000000, 0.000000000000000000 ) ) ;
#1797=ADVANCED_FACE ( 'NONE', ( #3358 ), #4407, .F. ) ;
#1806=LINE ( 'NONE', #4915, #3853 ) ;
#1808=ORIENTED_EDGE ( 'NONE', *, *, #1240, .F. ) ;
#1822=LINE ( 'NONE', #2531, #4714 ) ;
#1825=EDGE_LOOP ( 'NONE', ( #726, #3795, #3963 ) ) ;
#1831=CARTESIAN_POINT ( 'NONE',  ( 2.000000000000000000, 0.000000000000000000, 1.535500000000000087 ) ) ;
#1832=CARTESIAN_POINT ( 'NONE',  ( 2.000000000000000000, 0.8865213383406717051, 1.535499999999998533 ) ) ;
#1845=CYLINDRICAL_SURFACE ( 'NONE', #4582, 2.000000000000000888 ) ;
#1851=AXIS2_PLACEMENT_3D ( 'NONE', #2301, #401, #1927 ) ;
#1876=UNCERTAINTY_MEASURE_WITH_UNIT (LENGTH_MEASURE( 1.000000000000000082E-05 ), #4184, 'distance_accuracy_value', 'NONE');
#1880=DIRECTION ( 'NONE',  ( 0.000000000000000000, 0.000000000000000000, -1.000000000000000000 ) ) ;
#1885=CARTESIAN_POINT ( 'NONE',  ( 2.000000000000000000, 1.773042676681340968, -2.276824562219559311E-15 ) ) ;
#1887=PLANE ( 'NONE',  #3137 ) ;
#1890=ADVANCED_FACE ( 'NONE', ( #258 ), #3730, .T. ) ;
#1893=CARTESIAN_POINT ( 'NONE',  ( 2.000000000000000000, -0.8865213383406690406, 1.535500000000000975 ) ) ;
#1900=CARTESIAN_POINT ( 'NONE',  ( 23.61000000000001364, 0.000000000000000000, 2.000000000000000444 ) ) ;
#1904=ORIENTED_EDGE ( 'NONE', *, *, #1187, .T. ) ;
#1908=CARTESIAN_POINT ( 'NONE',  ( 2.000000000000000000, 1.773042676681340968, -2.276824562219559311E-15 ) ) ;
#1918=AXIS2_PLACEMENT_3D ( 'NONE', #1146, #2700, #1115 ) ;
#1925=VECTOR ( 'NONE', #3158, 1000.000000000000000 ) ;
#1927=DIRECTION ( 'NONE',  ( 0.000000000000000000, 0.000000000000000000, 1.000000000000000000 ) ) ;
#1939=AXIS2_PLACEMENT_3D ( 'NONE', #2200, #3006, #3397 ) ;
#1941=AXIS2_PLACEMENT_3D ( 'NONE', #2098, #4824, #4038 ) ;
#1944=ORIENTED_EDGE ( 'NONE', *, *, #4769, .T. ) ;
#1949=AXIS2_PLACEMENT_3D ( 'NONE', #163, #2126, #893 ) ;
#1950=ORIENTED_EDGE ( 'NONE', *, *, #3295, .T. ) ;
#1952=ADVANCED_FACE ( 'NONE', ( #4550 ), #1128, .T. ) ;
#1954=VECTOR ( 'NONE', #3101, 1000.000000000000000 ) ;
#1966=LINE ( 'NONE', #3789, #1954 ) ;
#1981=LINE ( 'NONE', #3487, #1615 ) ;
#1986=DIRECTION ( 'NONE',  ( 0.000000000000000000, -1.224646799147353207E-16, 1.000000000000000000 ) ) ;
#2001=PLANE ( 'NONE',  #4429 ) ;
#2005=DIRECTION ( 'NONE',  ( -1.000000000000000000, -0.000000000000000000, -0.000000000000000000 ) ) ;
#2009=MANIFOLD_SOLID_BREP ( 'Hex', #1546 ) ;
#2014=CARTESIAN_POINT ( 'NONE',  ( 0.000000000000000000, 1.773042676681340968, -2.276824562219559311E-15 ) ) ;
#2015=DIRECTION ( 'NONE',  ( 0.000000000000000000, 0.000000000000000000, -1.000000000000000000 ) ) ;
#2016=LINE ( 'NONE', #1265, #342 ) ;
#2030=DIRECTION ( 'NONE',  ( 0.000000000000000000, 0.000000000000000000, -1.000000000000000000 ) ) ;
#2042=ORIENTED_EDGE ( 'NONE', *, *, #1273, .T. ) ;
#2043=AXIS2_PLACEMENT_3D ( 'NONE', #4590, #534, #4557 ) ;
#2047=ADVANCED_FACE ( 'NONE', ( #2702 ), #3815, .T. ) ;
#2059=ORIENTED_EDGE ( 'NONE', *, *, #751, .F. ) ;
#2060=DIRECTION ( 'NONE',  ( 1.000000000000000000, 0.000000000000000000, 0.000000000000000000 ) ) ;
#2063=EDGE_LOOP ( 'NONE', ( #1549, #461, #4791, #3172 ) ) ;
#2065=DIRECTION ( 'NONE',  ( -1.000000000000000000, -0.000000000000000000, -0.000000000000000000 ) ) ;
#2095=ORIENTED_EDGE ( 'NONE', *, *, #2502, .T. ) ;
#2098=CARTESIAN_POINT ( 'NONE',  ( 0.000000000000000000, 0.000000000000000000, 0.000000000000000000 ) ) ;
#2103=AXIS2_PLACEMENT_3D ( 'NONE', #2232, #2259, #1880 ) ;
#2116=FILL_AREA_STYLE ('',( #1629 ) ) ;
#2122=EDGE_LOOP ( 'NONE', ( #2299, #2127, #1808 ) ) ;
#2126=DIRECTION ( 'NONE',  ( 1.000000000000000000, 0.000000000000000000, 0.000000000000000000 ) ) ;
#2127=ORIENTED_EDGE ( 'NONE', *, *, #4045, .F. ) ;
#2130=LINE ( 'NONE', #1365, #3134 ) ;
#2148=( GEOMETRIC_REPRESENTATION_CONTEXT ( 3 ) GLOBAL_UNCERTAINTY_ASSIGNED_CONTEXT ( ( #2386 ) ) GLOBAL_UNIT_ASSIGNED_CONTEXT ( ( #1732, #1356, #2520 ) ) REPRESENTATION_CONTEXT ( 'NONE', 'WORKASPACE' ) );
#2168=VECTOR ( 'NONE', #4066, 1000.000000000000000 ) ;
#2172=PLANE ( 'NONE',  #1314 ) ;
#2186=CIRCLE ( 'NONE', #2837, 1.535500000000000087 ) ;
#2196=DIRECTION ( 'NONE',  ( -1.000000000000000000, -0.000000000000000000, -0.000000000000000000 ) ) ;
#2198=ORIENTED_EDGE ( 'NONE', *, *, #4051, .F. ) ;
#2200=CARTESIAN_POINT ( 'NONE',  ( -31.74999999999995737, 0.000000000000000000, 0.000000000000000000 ) ) ;
#2205=EDGE_CURVE ( 'NONE', #934, #4080, #4095, .T. ) ;
#2206=VERTEX_POINT ( 'NONE', #4776 ) ;
#2218=LINE ( 'NONE', #1831, #1295 ) ;
#2230=DIRECTION ( 'NONE',  ( -0.000000000000000000, 0.8660254037844391517, 0.4999999999999990563 ) ) ;
#2232=CARTESIAN_POINT ( 'NONE',  ( 3.999999999999999112, 3.500000000000000000, 0.000000000000000000 ) ) ;
#2237=DIRECTION ( 'NONE',  ( 0.000000000000000000, 0.000000000000000000, 1.000000000000000000 ) ) ;
#2241=LINE ( 'NONE', #2948, #3938 ) ;
#2245=CIRCLE ( 'NONE', #3674, 1.535500000000000087 ) ;
#2251=AXIS2_PLACEMENT_3D ( 'NONE', #704, #3760, #1428 ) ;
#2259=DIRECTION ( 'NONE',  ( 1.000000000000000000, 0.000000000000000000, 0.000000000000000000 ) ) ;
#2267=LINE ( 'NONE', #1140, #1547 ) ;
#2288=FILL_AREA_STYLE ('',( #4844 ) ) ;
#2289=CARTESIAN_POINT ( 'NONE',  ( 2.000000000000000000, 1.773042676681340968, -2.276824562219559311E-15 ) ) ;
#2293=ORIENTED_EDGE ( 'NONE', *, *, #4030, .T. ) ;
#2299=ORIENTED_EDGE ( 'NONE', *, *, #3113, .F. ) ;
#2301=CARTESIAN_POINT ( 'NONE',  ( -31.74999999999995737, 0.000000000000000000, 0.000000000000000000 ) ) ;
#2311=( NAMED_UNIT ( * ) SI_UNIT ( $, .STERADIAN. ) SOLID_ANGLE_UNIT ( ) );
#2312=CARTESIAN_POINT ( 'NONE',  ( 2.000000000000000000, -1.502314598737159623E-15, -1.535500000000000087 ) ) ;
#2319=ORIENTED_EDGE ( 'NONE', *, *, #4172, .T. ) ;
#2327=CARTESIAN_POINT ( 'NONE',  ( 4.199999999999995737, 0.000000000000000000, 0.000000000000000000 ) ) ;
#2338=ORIENTED_EDGE ( 'NONE', *, *, #690, .T. ) ;
#2340=CARTESIAN_POINT ( 'NONE',  ( 0.000000000000000000, -0.8865213383406721492, -1.535499999999999199 ) ) ;
#2350=CARTESIAN_POINT ( 'NONE',  ( 0.1999999999999987899, 0.000000000000000000, 0.000000000000000000 ) ) ;
#2355=ORIENTED_EDGE ( 'NONE', *, *, #1187, .F. ) ;
#2367=ORIENTED_EDGE ( 'NONE', *, *, #1154, .T. ) ;
#2369=DIRECTION ( 'NONE',  ( 0.000000000000000000, 0.000000000000000000, -1.000000000000000000 ) ) ;
#2370=DIRECTION ( 'NONE',  ( 0.000000000000000000, -1.000000000000000000, 0.000000000000000000 ) ) ;
#2372=EDGE_LOOP ( 'NONE', ( #549, #473, #3545, #1272, #4448 ) ) ;
#2374=CARTESIAN_POINT ( 'NONE',  ( -31.74999999999995737, 0.000000000000000000, 2.000000000000000888 ) ) ;
#2383=EDGE_LOOP ( 'NONE', ( #1078, #3581, #2059 ) ) ;
#2384=ADVANCED_FACE ( 'NONE', ( #660 ), #4949, .F. ) ;
#2386=UNCERTAINTY_MEASURE_WITH_UNIT (LENGTH_MEASURE( 1.000000000000000082E-05 ), #1732, 'distance_accuracy_value', 'NONE');
#2387=DIRECTION ( 'NONE',  ( 0.000000000000000000, 0.000000000000000000, 1.000000000000000000 ) ) ;
#2395=ORIENTED_EDGE ( 'NONE', *, *, #4298, .F. ) ;
#2404=LINE ( 'NONE', #2807, #4396 ) ;
#2414=VECTOR ( 'NONE', #922, 1000.000000000000000 ) ;
#2419=DIRECTION ( 'NONE',  ( 0.000000000000000000, 0.000000000000000000, 1.000000000000000000 ) ) ;
#2445=DIRECTION ( 'NONE',  ( 0.000000000000000000, 0.000000000000000000, 1.000000000000000000 ) ) ;
#2447=CARTESIAN_POINT ( 'NONE',  ( 24.00000000000000000, 1.610000000000000098, 0.000000000000000000 ) ) ;
#2449=ADVANCED_FACE ( 'NONE', ( #4559 ), #1887, .F. ) ;
#2451=CARTESIAN_POINT ( 'NONE',  ( 3.999999999999999112, 0.000000000000000000, 0.000000000000000000 ) ) ;
#2466=ORIENTED_EDGE ( 'NONE', *, *, #1602, .F. ) ;
#2473=EDGE_CURVE ( 'NONE', #1518, #4266, #2218, .T. ) ;
#2474=ORIENTED_EDGE ( 'NONE', *, *, #1249, .F. ) ;
#2481=SHAPE_DEFINITION_REPRESENTATION ( #4819, #1326 ) ;
#2491=VERTEX_POINT ( 'NONE', #4637 ) ;
#2493=CARTESIAN_POINT ( 'NONE',  ( 0.000000000000000000, -1.773042676681340968, 2.059984127722458425E-15 ) ) ;
#2497=VECTOR ( 'NONE', #110, 1000.000000000000114 ) ;
#2502=EDGE_CURVE ( 'NONE', #1283, #4080, #1048, .T. ) ;
#2520=( NAMED_UNIT ( * ) SI_UNIT ( $, .STERADIAN. ) SOLID_ANGLE_UNIT ( ) );
#2524=PLANE ( 'NONE',  #666 ) ;
#2526=LINE ( 'NONE', #2862, #4569 ) ;
#2529=ORIENTED_EDGE ( 'NONE', *, *, #709, .T. ) ;
#2531=CARTESIAN_POINT ( 'NONE',  ( 2.000000000000000000, 0.8865213383406685965, -1.535500000000000753 ) ) ;
#2536=DIRECTION ( 'NONE',  ( 0.000000000000000000, 0.000000000000000000, 1.000000000000000000 ) ) ;
#2545=CYLINDRICAL_SURFACE ( 'NONE', #1939, 3.500000000000000000 ) ;
#2547=CARTESIAN_POINT ( 'NONE',  ( 2.000000000000000000, 0.000000000000000000, 0.000000000000000000 ) ) ;
#2548=ORIENTED_EDGE ( 'NONE', *, *, #709, .F. ) ;
#2550=DIRECTION ( 'NONE',  ( 0.000000000000000000, -0.5000000000000011102, -0.8660254037844379305 ) ) ;
#2558=FACE_OUTER_BOUND ( 'NONE', #2372, .T. ) ;
#2560=FACE_BOUND ( 'NONE', #1543, .T. ) ;
#2561=ORIENTED_EDGE ( 'NONE', *, *, #2626, .F. ) ;
#2575=ORIENTED_EDGE ( 'NONE', *, *, #2760, .T. ) ;
#2582=COLOUR_RGB ( '', 0.31764706, 0.68627451, 0.89019608) ;
#2585=EDGE_CURVE ( 'NONE', #4766, #934, #4244, .T. ) ;
#2589=AXIS2_PLACEMENT_3D ( 'NONE', #197, #1692, #925 ) ;
#2591=ORIENTED_EDGE ( 'NONE', *, *, #1278, .F. ) ;
#2598=CARTESIAN_POINT ( 'NONE',  ( 2.000000000000000000, -1.329782007511006281, -0.7677499999999984892 ) ) ;
#2602=CARTESIAN_POINT ( 'NONE',  ( 4.199999999999995737, 0.000000000000000000, 0.000000000000000000 ) ) ;
#2604=CARTESIAN_POINT ( 'NONE',  ( 0.000000000000000000, 4.163799117101000559E-16, -3.299999999999999822 ) ) ;
#2605=ORIENTED_EDGE ( 'NONE', *, *, #513, .F. ) ;
#2608=CARTESIAN_POINT ( 'NONE',  ( 0.000000000000000000, -0.8865213383406690406, 1.535500000000000975 ) ) ;
#2609=EDGE_LOOP ( 'NONE', ( #3090, #3803, #2605, #679, #1687 ) ) ;
#2613=CARTESIAN_POINT ( 'NONE',  ( 2.000000000000000000, 1.773042676681340968, -2.276824562219559311E-15 ) ) ;
#2617=SURFACE_SIDE_STYLE ('',( #4133 ) ) ;
#2622=ORIENTED_EDGE ( 'NONE', *, *, #4228, .T. ) ;
#2625=FACE_OUTER_BOUND ( 'NONE', #2609, .T. ) ;
#2626=EDGE_CURVE ( 'NONE', #392, #4266, #2186, .T. ) ;
#2628=ORIENTED_EDGE ( 'NONE', *, *, #3845, .F. ) ;
#2633=CARTESIAN_POINT ( 'NONE',  ( 4.199999999999995737, 0.000000000000000000, 0.000000000000000000 ) ) ;
#2641=VERTEX_POINT ( 'NONE', #539 ) ;
#2666=VECTOR ( 'NONE', #799, 1000.000000000000000 ) ;
#2683=ORIENTED_EDGE ( 'NONE', *, *, #3297, .F. ) ;
#2684=PRODUCT_DEFINITION ( 'UNKNOWN', '', #4463, #4938 ) ;
#2700=DIRECTION ( 'NONE',  ( 0.000000000000000000, 0.000000000000000000, 1.000000000000000000 ) ) ;
#2702=FACE_OUTER_BOUND ( 'NONE', #37, .T. ) ;
#2703=DIRECTION ( 'NONE',  ( 0.000000000000000000, 1.000000000000000000, -1.467581828789149532E-15 ) ) ;
#2704=ORIENTED_EDGE ( 'NONE', *, *, #1154, .F. ) ;
#2708=VERTEX_POINT ( 'NONE', #209 ) ;
#2717=CARTESIAN_POINT ( 'NONE',  ( 2.000000000000000000, 0.000000000000000000, 0.000000000000000000 ) ) ;
#2730=VECTOR ( 'NONE', #2864, 1000.000000000000227 ) ;
#2737=CONICAL_SURFACE ( 'NONE', #4811, 1.610000000000000098, 0.7853981633974647103 ) ;
#2741=ORIENTED_EDGE ( 'NONE', *, *, #228, .T. ) ;
#2744=AXIS2_PLACEMENT_3D ( 'NONE', #3706, #2230, #1778 ) ;
#2759=CARTESIAN_POINT ( 'NONE',  ( -31.74999999999995737, 0.000000000000000000, 0.000000000000000000 ) ) ;
#2760=EDGE_CURVE ( 'NONE', #3989, #3847, #176, .T. ) ;
#2770=ORIENTED_EDGE ( 'NONE', *, *, #4437, .T. ) ;
#2783=ADVANCED_FACE ( 'NONE', ( #560, #956 ), #358, .T. ) ;
#2784=CARTESIAN_POINT ( 'NONE',  ( 4.199999999999995737, 0.000000000000000000, 0.000000000000000000 ) ) ;
#2788=ADVANCED_FACE ( 'NONE', ( #4078 ), #3731, .T. ) ;
#2790=SURFACE_STYLE_FILL_AREA ( #2116 ) ;
#2794=EDGE_LOOP ( 'NONE', ( #2355, #2926, #702, #4624, #3618 ) ) ;
#2796=CARTESIAN_POINT ( 'NONE',  ( 0.1999999999999987899, 4.041334437186265510E-16, -3.299999999999999822 ) ) ;
#2797=DIRECTION ( 'NONE',  ( -1.000000000000000000, -0.000000000000000000, -0.000000000000000000 ) ) ;
#2803=EDGE_CURVE ( 'NONE', #3027, #3976, #1806, .T. ) ;
#2807=CARTESIAN_POINT ( 'NONE',  ( 2.000000000000000000, -0.8865213383406690406, 1.535500000000000975 ) ) ;
#2808=AXIS2_PLACEMENT_3D ( 'NONE', #2602, #2904, #4420 ) ;
#2817=AXIS2_PLACEMENT_3D ( 'NONE', #2451, #988, #3615 ) ;
#2821=CARTESIAN_POINT ( 'NONE',  ( 2.000000000000000000, -1.773042676681340968, 2.059984127722458425E-15 ) ) ;
#2827=VERTEX_POINT ( 'NONE', #4152 ) ;
#2837=AXIS2_PLACEMENT_3D ( 'NONE', #2717, #4232, #4264 ) ;
#2855=DIRECTION ( 'NONE',  ( 0.000000000000000000, -0.4999999999999993339, 0.8660254037844389297 ) ) ;
#2862=CARTESIAN_POINT ( 'NONE',  ( 2.000000000000000000, -0.8865213383406721492, -1.535499999999999199 ) ) ;
#2863=DIRECTION ( 'NONE',  ( -1.000000000000000000, -0.000000000000000000, -0.000000000000000000 ) ) ;
#2864=DIRECTION ( 'NONE',  ( 0.000000000000000000, -0.5000000000000008882, -0.8660254037844380415 ) ) ;
#2871=CARTESIAN_POINT ( 'NONE',  ( 0.1999999999999987899, 0.000000000000000000, 0.000000000000000000 ) ) ;
#2873=CARTESIAN_POINT ( 'NONE',  ( 0.000000000000000000, 0.8865213383406717051, 1.535499999999998533 ) ) ;
#2877=DIRECTION ( 'NONE',  ( 1.000000000000000000, 0.000000000000000000, 0.000000000000000000 ) ) ;
#2879=FACE_OUTER_BOUND ( 'NONE', #3495, .T. ) ;
#2889=CONICAL_SURFACE ( 'NONE', #4640, 1.535500000000000087, 1.047197551196590748 ) ;
#2893=CIRCLE ( 'NONE', #3601, 0.2000000000000000944 ) ;
#2904=DIRECTION ( 'NONE',  ( 1.000000000000000000, 0.000000000000000000, 0.000000000000000000 ) ) ;
#2906=LINE ( 'NONE', #4421, #2730 ) ;
#2910=ORIENTED_EDGE ( 'NONE', *, *, #2205, .F. ) ;
#2920=DIRECTION ( 'NONE',  ( 0.000000000000000000, 0.000000000000000000, -1.000000000000000000 ) ) ;
#2926=ORIENTED_EDGE ( 'NONE', *, *, #3052, .F. ) ;
#2935=ADVANCED_FACE ( 'NONE', ( #2558 ), #3017, .F. ) ;
#2948=CARTESIAN_POINT ( 'NONE',  ( 2.000000000000000000, 1.773042676681340968, -2.276824562219559311E-15 ) ) ;
#2952=EDGE_CURVE ( 'NONE', #4685, #675, #4565, .T. ) ;
#2965=LINE ( 'NONE', #3680, #4094 ) ;
#2970=FACE_OUTER_BOUND ( 'NONE', #482, .T. ) ;
#2994=DIRECTION ( 'NONE',  ( 0.000000000000000000, 0.5000000000000011102, 0.8660254037844379305 ) ) ;
#3003=ORIENTED_EDGE ( 'NONE', *, *, #751, .T. ) ;
#3006=DIRECTION ( 'NONE',  ( -1.000000000000000000, -0.000000000000000000, -0.000000000000000000 ) ) ;
#3017=PLANE ( 'NONE',  #1696 ) ;
#3022=( NAMED_UNIT ( * ) PLANE_ANGLE_UNIT ( ) SI_UNIT ( $, .RADIAN. ) );
#3027=VERTEX_POINT ( 'NONE', #74 ) ;
#3038=DIRECTION ( 'NONE',  ( 0.000000000000000000, -0.4999999999999993339, 0.8660254037844389297 ) ) ;
#3052=EDGE_CURVE ( 'NONE', #2206, #4462, #1981, .T. ) ;
#3065=VECTOR ( 'NONE', #2855, 1000.000000000000114 ) ;
#3073=ORIENTED_EDGE ( 'NONE', *, *, #2803, .F. ) ;
#3079=EDGE_LOOP ( 'NONE', ( #4632, #255, #2367, #2591 ) ) ;
#3090=ORIENTED_EDGE ( 'NONE', *, *, #3748, .T. ) ;
#3101=DIRECTION ( 'NONE',  ( -0.5000000000000061062, 1.060575238724902601E-16, -0.8660254037844351549 ) ) ;
#3113=EDGE_CURVE ( 'NONE', #2206, #3948, #3535, .T. ) ;
#3121=CARTESIAN_POINT ( 'NONE',  ( 2.886521338340684917, 0.000000000000000000, 0.000000000000000000 ) ) ;
#3134=VECTOR ( 'NONE', #3256, 1000.000000000000000 ) ;
#3136=ORIENTED_EDGE ( 'NONE', *, *, #690, .F. ) ;
#3137=AXIS2_PLACEMENT_3D ( 'NONE', #1908, #3788, #311 ) ;
#3139=CARTESIAN_POINT ( 'NONE',  ( 2.000000000000000000, 0.000000000000000000, 0.000000000000000000 ) ) ;
#3146=PRODUCT_CONTEXT ( 'NONE', #4288, 'mechanical' ) ;
#3147=CARTESIAN_POINT ( 'NONE',  ( 2.000000000000000000, -0.8865213383406690406, 1.535500000000000975 ) ) ;
#3158=DIRECTION ( 'NONE',  ( -1.000000000000000000, -0.000000000000000000, -0.000000000000000000 ) ) ;
#3172=ORIENTED_EDGE ( 'NONE', *, *, #1107, .F. ) ;
#3175=EDGE_CURVE ( 'NONE', #1323, #1525, #2526, .T. ) ;
#3176=DIRECTION ( 'NONE',  ( -0.5000000000000061062, 0.000000000000000000, 0.8660254037844351549 ) ) ;
#3178=EDGE_LOOP ( 'NONE', ( #3612, #2628, #2095, #2910 ) ) ;
#3194=LINE ( 'NONE', #1318, #3065 ) ;
#3197=ORIENTED_EDGE ( 'NONE', *, *, #1155, .F. ) ;
#3210=ADVANCED_FACE ( 'NONE', ( #1015 ), #2545, .T. ) ;
#3216=AXIS2_PLACEMENT_3D ( 'NONE', #2350, #2877, #632 ) ;
#3227=DIRECTION ( 'NONE',  ( 0.000000000000000000, 0.4999999999999990008, -0.8660254037844391517 ) ) ;
#3228=STYLED_ITEM ( 'NONE', ( #4307 ), #2009 ) ;
#3245=CIRCLE ( 'NONE', #3877, 2.200000000000001066 ) ;
#3249=DIRECTION ( 'NONE',  ( 0.000000000000000000, -0.5000000000000011102, -0.8660254037844379305 ) ) ;
#3253=EDGE_LOOP ( 'NONE', ( #2293, #1363, #663, #4818 ) ) ;
#3256=DIRECTION ( 'NONE',  ( -1.000000000000000000, -0.000000000000000000, -0.000000000000000000 ) ) ;
#3267=EDGE_CURVE ( 'NONE', #7, #519, #2241, .T. ) ;
#3278=DIRECTION ( 'NONE',  ( 0.000000000000000000, -1.000000000000000000, 9.783878858594330870E-16 ) ) ;
#3283=FACE_OUTER_BOUND ( 'NONE', #3178, .T. ) ;
#3289=ORIENTED_EDGE ( 'NONE', *, *, #1176, .F. ) ;
#3291=CARTESIAN_POINT ( 'NONE',  ( 0.1999999999999987899, 0.000000000000000000, 3.500000000000000000 ) ) ;
#3295=EDGE_CURVE ( 'NONE', #1595, #392, #4118, .T. ) ;
#3296=CIRCLE ( 'NONE', #3605, 0.2000000000000000944 ) ;
#3297=EDGE_CURVE ( 'NONE', #3361, #4023, #4252, .T. ) ;
#3311=ORIENTED_EDGE ( 'NONE', *, *, #2502, .F. ) ;
#3314=DIRECTION ( 'NONE',  ( -1.000000000000000000, -0.000000000000000000, -0.000000000000000000 ) ) ;
#3340=FACE_OUTER_BOUND ( 'NONE', #4944, .T. ) ;
#3353=DIRECTION ( 'NONE',  ( -1.000000000000000000, -0.000000000000000000, -0.000000000000000000 ) ) ;
#3358=FACE_OUTER_BOUND ( 'NONE', #828, .T. ) ;
#3361=VERTEX_POINT ( 'NONE', #1900 ) ;
#3383=VECTOR ( 'NONE', #2005, 1000.000000000000000 ) ;
#3384=ADVANCED_FACE ( 'NONE', ( #3430 ), #438, .F. ) ;
#3397=DIRECTION ( 'NONE',  ( 0.000000000000000000, 0.000000000000000000, 1.000000000000000000 ) ) ;
#3402=UNCERTAINTY_MEASURE_WITH_UNIT (LENGTH_MEASURE( 1.000000000000000082E-05 ), #4707, 'distance_accuracy_value', 'NONE');
#3430=FACE_OUTER_BOUND ( 'NONE', #2122, .T. ) ;
#3436=SHAPE_REPRESENTATION_RELATIONSHIP ( 'NONE' , 'NONE' ,  #1326, #1407 ) ;
#3437=DIRECTION ( 'NONE',  ( -1.000000000000000000, -0.000000000000000000, -0.000000000000000000 ) ) ;
#3440=ORIENTED_EDGE ( 'NONE', *, *, #1784, .F. ) ;
#3441=AXIS2_PLACEMENT_3D ( 'NONE', #2327, #4626, #899 ) ;
#3453=TOROIDAL_SURFACE ( 'NONE', #734, 3.299999999999999822, 0.2000000000000000111 ) ;
#3474=EDGE_LOOP ( 'NONE', ( #1564, #198 ) ) ;
#3476=DIRECTION ( 'NONE',  ( 0.000000000000000000, 0.000000000000000000, -1.000000000000000000 ) ) ;
#3481=DIRECTION ( 'NONE',  ( 0.000000000000000000, 1.000000000000000000, -1.467581828789149532E-15 ) ) ;
#3487=CARTESIAN_POINT ( 'NONE',  ( 2.000000000000000000, -1.773042676681340968, 2.059984127722458425E-15 ) ) ;
#3495=EDGE_LOOP ( 'NONE', ( #4555, #1091, #1113, #3136 ) ) ;
#3508=EDGE_CURVE ( 'NONE', #4266, #3027, #4417, .T. ) ;
#3527=CIRCLE ( 'NONE', #3216, 3.500000000000000000 ) ;
#3528=EDGE_CURVE ( 'NONE', #3847, #1283, #488, .T. ) ;
#3530=CARTESIAN_POINT ( 'NONE',  ( 2.000000000000000000, 1.773042676681340968, -2.276824562219559311E-15 ) ) ;
#3535=LINE ( 'NONE', #106, #12 ) ;
#3545=ORIENTED_EDGE ( 'NONE', *, *, #4181, .F. ) ;
#3555=CARTESIAN_POINT ( 'NONE',  ( 0.000000000000000000, 1.773042676681340968, -2.276824562219559311E-15 ) ) ;
#3569=CARTESIAN_POINT ( 'NONE',  ( 2.000000000000000000, 0.8865213383406685965, -1.535500000000000753 ) ) ;
#3577=ORIENTED_EDGE ( 'NONE', *, *, #2585, .T. ) ;
#3579=SURFACE_STYLE_USAGE ( .BOTH. , #4763 ) ;
#3581=ORIENTED_EDGE ( 'NONE', *, *, #1758, .F. ) ;
#3584=CARTESIAN_POINT ( 'NONE',  ( 24.00000000000000000, 0.000000000000000000, 0.000000000000000000 ) ) ;
#3588=ORIENTED_EDGE ( 'NONE', *, *, #1278, .T. ) ;
#3593=VECTOR ( 'NONE', #2863, 1000.000000000000000 ) ;
#3601=AXIS2_PLACEMENT_3D ( 'NONE', #1540, #1270, #3949 ) ;
#3605=AXIS2_PLACEMENT_3D ( 'NONE', #703, #4868, #4157 ) ;
#3612=ORIENTED_EDGE ( 'NONE', *, *, #2585, .F. ) ;
#3615=DIRECTION ( 'NONE',  ( 0.000000000000000000, 0.000000000000000000, -1.000000000000000000 ) ) ;
#3618=ORIENTED_EDGE ( 'NONE', *, *, #3175, .T. ) ;
#3621=DIRECTION ( 'NONE',  ( 1.000000000000000000, 0.000000000000000000, 0.000000000000000000 ) ) ;
#3635=ORIENTED_EDGE ( 'NONE', *, *, #3175, .F. ) ;
#3644=CARTESIAN_POINT ( 'NONE',  ( 23.61000000000001364, 0.000000000000000000, 0.000000000000000000 ) ) ;
#3645=ORIENTED_EDGE ( 'NONE', *, *, #99, .F. ) ;
#3665=DIRECTION ( 'NONE',  ( -1.000000000000000000, -0.000000000000000000, -0.000000000000000000 ) ) ;
#3674=AXIS2_PLACEMENT_3D ( 'NONE', #595, #3665, #615 ) ;
#3680=CARTESIAN_POINT ( 'NONE',  ( 2.000000000000000000, -0.8865213383406690406, 1.535500000000000975 ) ) ;
#3681=ADVANCED_FACE ( 'NONE', ( #1440 ), #1845, .T. ) ;
#3685=TOROIDAL_SURFACE ( 'NONE', #3767, 3.299999999999999822, 0.2000000000000000111 ) ;
#3687=DIRECTION ( 'NONE',  ( 0.000000000000000000, 0.000000000000000000, 1.000000000000000000 ) ) ;
#3706=CARTESIAN_POINT ( 'NONE',  ( 2.000000000000000000, -1.773042676681340968, 2.059984127722458425E-15 ) ) ;
#3708=DIRECTION ( 'NONE',  ( -1.000000000000000000, 0.000000000000000000, -0.000000000000000000 ) ) ;
#3710=CIRCLE ( 'NONE', #1553, 1.535500000000000087 ) ;
#3711=CARTESIAN_POINT ( 'NONE',  ( 2.000000000000000000, 1.773042676681340968, -2.276824562219559311E-15 ) ) ;
#3719=DIRECTION ( 'NONE',  ( 0.000000000000000000, 0.000000000000000000, 1.000000000000000000 ) ) ;
#3730=PLANE ( 'NONE',  #2744 ) ;
#3731=PLANE ( 'NONE',  #727 ) ;
#3734=DIRECTION ( 'NONE',  ( -1.000000000000000000, -0.000000000000000000, -0.000000000000000000 ) ) ;
#3741=ORIENTED_EDGE ( 'NONE', *, *, #1240, .T. ) ;
#3748=EDGE_CURVE ( 'NONE', #297, #4198, #1251, .T. ) ;
#3752=DIRECTION ( 'NONE',  ( 0.000000000000000000, -0.8660254037844390407, -0.4999999999999993339 ) ) ;
#3760=DIRECTION ( 'NONE',  ( 1.000000000000000000, 0.000000000000000000, 0.000000000000000000 ) ) ;
#3761=CARTESIAN_POINT ( 'NONE',  ( 23.61000000000001364, 2.449293598294707400E-16, -2.000000000000000444 ) ) ;
#3763=ORIENTED_EDGE ( 'NONE', *, *, #3528, .T. ) ;
#3764=DIRECTION ( 'NONE',  ( -1.000000000000000000, -0.000000000000000000, -0.000000000000000000 ) ) ;
#3767=AXIS2_PLACEMENT_3D ( 'NONE', #1137, #4185, #3687 ) ;
#3773=CARTESIAN_POINT ( 'NONE',  ( 2.000000000000000000, -1.329782007511004727, 0.7677500000000014868 ) ) ;
#3778=ORIENTED_EDGE ( 'NONE', *, *, #1576, .F. ) ;
#3784=CONICAL_SURFACE ( 'NONE', #2589, 1.610000000000000098, 0.7853981633974647103 ) ;
#3788=DIRECTION ( 'NONE',  ( 1.000000000000000000, 0.000000000000000000, 0.000000000000000000 ) ) ;
#3789=CARTESIAN_POINT ( 'NONE',  ( 2.000000000000000000, 1.880445160090761061E-16, -1.535500000000000087 ) ) ;
#3792=VECTOR ( 'NONE', #2550, 1000.000000000000114 ) ;
#3795=ORIENTED_EDGE ( 'NONE', *, *, #4523, .T. ) ;
#3798=ORIENTED_EDGE ( 'NONE', *, *, #2952, .T. ) ;
#3803=ORIENTED_EDGE ( 'NONE', *, *, #4228, .F. ) ;
#3806=SURFACE_STYLE_USAGE ( .BOTH. , #2617 ) ;
#3811=ADVANCED_FACE ( 'NONE', ( #2879 ), #3784, .T. ) ;
#3815=CYLINDRICAL_SURFACE ( 'NONE', #739, 3.500000000000000000 ) ;
#3832=CIRCLE ( 'NONE', #2808, 2.000000000000000888 ) ;
#3834=CARTESIAN_POINT ( 'NONE',  ( 0.1999999999999987899, 0.000000000000000000, 3.299999999999999822 ) ) ;
#3845=EDGE_CURVE ( 'NONE', #1283, #4766, #24, .T. ) ;
#3847=VERTEX_POINT ( 'NONE', #4753 ) ;
#3853=VECTOR ( 'NONE', #3038, 1000.000000000000114 ) ;
#3875=DIRECTION ( 'NONE',  ( 0.000000000000000000, 0.000000000000000000, 1.000000000000000000 ) ) ;
#3877=AXIS2_PLACEMENT_3D ( 'NONE', #4104, #1770, #1720 ) ;
#3883=ORIENTED_EDGE ( 'NONE', *, *, #776, .T. ) ;
#3892=ORIENTED_EDGE ( 'NONE', *, *, #3508, .F. ) ;
#3909=ORIENTED_EDGE ( 'NONE', *, *, #4051, .T. ) ;
#3931=CIRCLE ( 'NONE', #1765, 1.535500000000000087 ) ;
#3935=CARTESIAN_POINT ( 'NONE',  ( -31.74999999999995737, 0.000000000000000000, 3.500000000000000000 ) ) ;
#3938=VECTOR ( 'NONE', #368, 1000.000000000000000 ) ;
#3948=VERTEX_POINT ( 'NONE', #2598 ) ;
#3949=DIRECTION ( 'NONE',  ( 0.000000000000000000, 0.000000000000000000, -1.000000000000000000 ) ) ;
#3956=EDGE_LOOP ( 'NONE', ( #1153, #3440 ) ) ;
#3963=ORIENTED_EDGE ( 'NONE', *, *, #228, .F. ) ;
#3966=DIRECTION ( 'NONE',  ( 0.000000000000000000, 0.000000000000000000, -1.000000000000000000 ) ) ;
#3976=VERTEX_POINT ( 'NONE', #1832 ) ;
#3983=EDGE_LOOP ( 'NONE', ( #2548, #2395, #1950, #4238, #435 ) ) ;
#3984=CARTESIAN_POINT ( 'NONE',  ( 2.000000000000000000, 0.000000000000000000, 0.000000000000000000 ) ) ;
#3985=ADVANCED_FACE ( 'NONE', ( #990 ), #2524, .T. ) ;
#3989=VERTEX_POINT ( 'NONE', #312 ) ;
#3991=CARTESIAN_POINT ( 'NONE',  ( 24.00000000000000000, 0.000000000000000000, 1.610000000000000098 ) ) ;
#4014=LINE ( 'NONE', #3991, #1552 ) ;
#4023=VERTEX_POINT ( 'NONE', #3761 ) ;
#4026=ADVANCED_FACE ( 'NONE', ( #1460 ), #2172, .F. ) ;
#4030=EDGE_CURVE ( 'NONE', #3847, #3989, #28, .T. ) ;
#4038=DIRECTION ( 'NONE',  ( 0.000000000000000000, 0.000000000000000000, 1.000000000000000000 ) ) ;
#4045=EDGE_CURVE ( 'NONE', #392, #2206, #2267, .T. ) ;
#4048=CARTESIAN_POINT ( 'NONE',  ( 2.000000000000000000, 0.000000000000000000, 0.000000000000000000 ) ) ;
#4051=EDGE_CURVE ( 'NONE', #1518, #1504, #1966, .T. ) ;
#4066=DIRECTION ( 'NONE',  ( 0.000000000000000000, -1.000000000000000000, 9.783878858594330870E-16 ) ) ;
#4078=FACE_OUTER_BOUND ( 'NONE', #1493, .T. ) ;
#4080=VERTEX_POINT ( 'NONE', #366 ) ;
#4090=DIRECTION ( 'NONE',  ( 0.000000000000000000, 1.000000000000000000, -9.783878858594330870E-16 ) ) ;
#4093=AXIS2_PLACEMENT_3D ( 'NONE', #1793, #3764, #4952 ) ;
#4094=VECTOR ( 'NONE', #3314, 1000.000000000000000 ) ;
#4095=CIRCLE ( 'NONE', #1941, 3.299999999999999822 ) ;
#4104=CARTESIAN_POINT ( 'NONE',  ( 3.999999999999999112, 0.000000000000000000, 0.000000000000000000 ) ) ;
#4105=EDGE_LOOP ( 'NONE', ( #4428, #1792, #1375, #2704 ) ) ;
#4109=CARTESIAN_POINT ( 'NONE',  ( 0.000000000000000000, 0.000000000000000000, 0.000000000000000000 ) ) ;
#4115=CARTESIAN_POINT ( 'NONE',  ( 2.000000000000000000, -0.8865213383406690406, 1.535500000000000975 ) ) ;
#4118=LINE ( 'NONE', #4489, #426 ) ;
#4121=ADVANCED_FACE ( 'NONE', ( #958 ), #1684, .T. ) ;
#4129=DIRECTION ( 'NONE',  ( 0.000000000000000000, 0.4999999999999993339, -0.8660254037844390407 ) ) ;
#4133=SURFACE_STYLE_FILL_AREA ( #2288 ) ;
#4152=CARTESIAN_POINT ( 'NONE',  ( 3.999999999999997335, 0.000000000000000000, -2.200000000000001066 ) ) ;
#4157=DIRECTION ( 'NONE',  ( 0.000000000000000000, 1.224646799147353207E-16, 1.000000000000000000 ) ) ;
#4170=DIRECTION ( 'NONE',  ( 0.000000000000000000, -0.5000000000000011102, -0.8660254037844379305 ) ) ;
#4172=EDGE_CURVE ( 'NONE', #7, #3027, #3194, .T. ) ;
#4181=EDGE_CURVE ( 'NONE', #497, #2491, #863, .T. ) ;
#4184=( LENGTH_UNIT ( ) NAMED_UNIT ( * ) SI_UNIT ( .MILLI., .METRE. ) );
#4185=DIRECTION ( 'NONE',  ( -1.000000000000000000, -0.000000000000000000, -0.000000000000000000 ) ) ;
#4198=VERTEX_POINT ( 'NONE', #2873 ) ;
#4205=FACE_OUTER_BOUND ( 'NONE', #4273, .T. ) ;
#4225=LINE ( 'NONE', #4942, #2666 ) ;
#4228=EDGE_CURVE ( 'NONE', #3976, #4198, #2016, .T. ) ;
#4232=DIRECTION ( 'NONE',  ( -1.000000000000000000, -0.000000000000000000, -0.000000000000000000 ) ) ;
#4236=ORIENTED_EDGE ( 'NONE', *, *, #1602, .T. ) ;
#4238=ORIENTED_EDGE ( 'NONE', *, *, #4045, .T. ) ;
#4244=CIRCLE ( 'NONE', #572, 0.2000000000000000944 ) ;
#4252=CIRCLE ( 'NONE', #4093, 2.000000000000000444 ) ;
#4262=LINE ( 'NONE', #838, #92 ) ;
#4264=DIRECTION ( 'NONE',  ( 0.000000000000000000, 0.000000000000000000, 1.000000000000000000 ) ) ;
#4266=VERTEX_POINT ( 'NONE', #1382 ) ;
#4271=CIRCLE ( 'NONE', #2043, 3.299999999999999822 ) ;
#4273=EDGE_LOOP ( 'NONE', ( #1486, #1579, #1517 ) ) ;
#4288=APPLICATION_CONTEXT ( 'automotive_design' ) ;
#4290=ADVANCED_FACE ( 'NONE', ( #2560, #1352 ), #1056, .T. ) ;
#4298=EDGE_CURVE ( 'NONE', #1595, #297, #2965, .T. ) ;
#4307=PRESENTATION_STYLE_ASSIGNMENT (( #3579 ) ) ;
#4309=DIRECTION ( 'NONE',  ( -1.000000000000000000, -0.000000000000000000, -0.000000000000000000 ) ) ;
#4312=LINE ( 'NONE', #2014, #2497 ) ;
#4316=ORIENTED_EDGE ( 'NONE', *, *, #2626, .T. ) ;
#4318=EDGE_LOOP ( 'NONE', ( #3883, #3635, #3197, #1601, #1944 ) ) ;
#4322=CIRCLE ( 'NONE', #1600, 2.000000000000000444 ) ;
#4325=FACE_OUTER_BOUND ( 'NONE', #4105, .T. ) ;
#4332=CIRCLE ( 'NONE', #817, 1.610000000000000098 ) ;
#4336=VECTOR ( 'NONE', #3249, 1000.000000000000114 ) ;
#4338=DIRECTION ( 'NONE',  ( 0.000000000000000000, 0.4999999999999990008, -0.8660254037844391517 ) ) ;
#4350=AXIS2_PLACEMENT_3D ( 'NONE', #662, #2196, #3719 ) ;
#4388=CARTESIAN_POINT ( 'NONE',  ( 2.000000000000000000, -0.8865213383406690406, 1.535500000000000975 ) ) ;
#4396=VECTOR ( 'NONE', #3481, 1000.000000000000000 ) ;
#4407=CONICAL_SURFACE ( 'NONE', #896, 1.535500000000000087, 1.047197551196590748 ) ;
#4417=CIRCLE ( 'NONE', #4662, 1.535500000000000087 ) ;
#4420=DIRECTION ( 'NONE',  ( 0.000000000000000000, 0.000000000000000000, -1.000000000000000000 ) ) ;
#4421=CARTESIAN_POINT ( 'NONE',  ( 0.000000000000000000, -0.8865213383406690406, 1.535500000000000975 ) ) ;
#4428=ORIENTED_EDGE ( 'NONE', *, *, #2952, .F. ) ;
#4429=AXIS2_PLACEMENT_3D ( 'NONE', #3530, #2060, #4682 ) ;
#4430=DIRECTION ( 'NONE',  ( -1.000000000000000000, -0.000000000000000000, -0.000000000000000000 ) ) ;
#4434=CARTESIAN_POINT ( 'NONE',  ( 2.000000000000000000, -0.8865213383406721492, -1.535499999999999199 ) ) ;
#4437=EDGE_CURVE ( 'NONE', #1327, #4023, #4225, .T. ) ;
#4441=FACE_OUTER_BOUND ( 'NONE', #22, .T. ) ;
#4442=APPLICATION_CONTEXT ( 'automotive_design' ) ;
#4448=ORIENTED_EDGE ( 'NONE', *, *, #3267, .T. ) ;
#4454=( GEOMETRIC_REPRESENTATION_CONTEXT ( 3 ) GLOBAL_UNCERTAINTY_ASSIGNED_CONTEXT ( ( #1876 ) ) GLOBAL_UNIT_ASSIGNED_CONTEXT ( ( #4184, #3022, #2311 ) ) REPRESENTATION_CONTEXT ( 'NONE', 'WORKASPACE' ) );
#4462=VERTEX_POINT ( 'NONE', #1397 ) ;
#4463=PRODUCT_DEFINITION_FORMATION_WITH_SPECIFIED_SOURCE ( 'ANY', '', #613, .NOT_KNOWN. ) ;
#4471=CARTESIAN_POINT ( 'NONE',  ( 0.000000000000000000, 0.8865213383406685965, -1.535500000000000753 ) ) ;
#4472=ORIENTED_EDGE ( 'NONE', *, *, #2473, .F. ) ;
#4482=PLANE ( 'NONE',  #118 ) ;
#4489=CARTESIAN_POINT ( 'NONE',  ( 2.000000000000000000, -0.8865213383406690406, 1.535500000000000975 ) ) ;
#4491=DIRECTION ( 'NONE',  ( -0.000000000000000000, 1.467581828789149729E-15, 1.000000000000000000 ) ) ;
#4504=ORIENTED_EDGE ( 'NONE', *, *, #776, .F. ) ;
#4511=DIRECTION ( 'NONE',  ( 0.000000000000000000, -9.783878858594330870E-16, -1.000000000000000000 ) ) ;
#4523=EDGE_CURVE ( 'NONE', #2491, #1504, #1822, .T. ) ;
#4526=CARTESIAN_POINT ( 'NONE',  ( 2.000000000000000000, 1.773042676681340968, -2.276824562219559311E-15 ) ) ;
#4550=FACE_OUTER_BOUND ( 'NONE', #2063, .T. ) ;
#4555=ORIENTED_EDGE ( 'NONE', *, *, #4437, .F. ) ;
#4557=DIRECTION ( 'NONE',  ( 0.000000000000000000, 0.000000000000000000, 1.000000000000000000 ) ) ;
#4559=FACE_OUTER_BOUND ( 'NONE', #1404, .T. ) ;
#4562=ORIENTED_EDGE ( 'NONE', *, *, #4030, .F. ) ;
#4565=CIRCLE ( 'NONE', #256, 2.000000000000000888 ) ;
#4569=VECTOR ( 'NONE', #199, 1000.000000000000000 ) ;
#4582=AXIS2_PLACEMENT_3D ( 'NONE', #2759, #3353, #3875 ) ;
#4590=CARTESIAN_POINT ( 'NONE',  ( 0.000000000000000000, 0.000000000000000000, 0.000000000000000000 ) ) ;
#4624=ORIENTED_EDGE ( 'NONE', *, *, #1758, .T. ) ;
#4626=DIRECTION ( 'NONE',  ( 1.000000000000000000, 0.000000000000000000, 0.000000000000000000 ) ) ;
#4632=ORIENTED_EDGE ( 'NONE', *, *, #1415, .F. ) ;
#4637=CARTESIAN_POINT ( 'NONE',  ( 2.000000000000000000, 0.8865213383406685965, -1.535500000000000753 ) ) ;
#4640=AXIS2_PLACEMENT_3D ( 'NONE', #2547, #4853, #638 ) ;
#4641=ORIENTED_EDGE ( 'NONE', *, *, #2760, .F. ) ;
#4654=VECTOR ( 'NONE', #4338, 1000.000000000000227 ) ;
#4661=ORIENTED_EDGE ( 'NONE', *, *, #463, .F. ) ;
#4662=AXIS2_PLACEMENT_3D ( 'NONE', #3139, #4683, #2387 ) ;
#4671=EDGE_LOOP ( 'NONE', ( #1194, #3588 ) ) ;
#4678=LINE ( 'NONE', #1324, #3593 ) ;
#4679=CARTESIAN_POINT ( 'NONE',  ( 2.000000000000000000, 1.329782007511004727, -0.7677500000000019309 ) ) ;
#4680=ORIENTED_EDGE ( 'NONE', *, *, #3295, .F. ) ;
#4681=ORIENTED_EDGE ( 'NONE', *, *, #513, .T. ) ;
#4682=DIRECTION ( 'NONE',  ( 0.000000000000000000, 0.000000000000000000, -1.000000000000000000 ) ) ;
#4683=DIRECTION ( 'NONE',  ( -1.000000000000000000, -0.000000000000000000, -0.000000000000000000 ) ) ;
#4685=VERTEX_POINT ( 'NONE', #1491 ) ;
#4707=( LENGTH_UNIT ( ) NAMED_UNIT ( * ) SI_UNIT ( .MILLI., .METRE. ) );
#4714=VECTOR ( 'NONE', #3278, 1000.000000000000000 ) ;
#4735=AXIS2_PLACEMENT_3D ( 'NONE', #3984, #1349, #2445 ) ;
#4753=CARTESIAN_POINT ( 'NONE',  ( 4.000000000000003553, 0.000000000000000000, 3.500000000000000000 ) ) ;
#4757=CARTESIAN_POINT ( 'NONE',  ( 0.000000000000000000, 0.8865213383406685965, -1.535500000000000753 ) ) ;
#4760=DIRECTION ( 'NONE',  ( 0.000000000000000000, 0.000000000000000000, 1.000000000000000000 ) ) ;
#4763=SURFACE_SIDE_STYLE ('',( #2790 ) ) ;
#4766=VERTEX_POINT ( 'NONE', #1717 ) ;
#4769=EDGE_CURVE ( 'NONE', #2491, #313, #4678, .T. ) ;
#4776=CARTESIAN_POINT ( 'NONE',  ( 2.000000000000000000, -1.773042676681340968, 2.059984127722458425E-15 ) ) ;
#4790=ADVANCED_FACE ( 'NONE', ( #1253 ), #1033, .F. ) ;
#4791=ORIENTED_EDGE ( 'NONE', *, *, #4921, .T. ) ;
#4792=ORIENTED_EDGE ( 'NONE', *, *, #3267, .F. ) ;
#4794=CARTESIAN_POINT ( 'NONE',  ( 2.000000000000000000, 0.000000000000000000, 0.000000000000000000 ) ) ;
#4811=AXIS2_PLACEMENT_3D ( 'NONE', #1034, #3734, #2237 ) ;
#4813=LINE ( 'NONE', #2821, #4654 ) ;
#4818=ORIENTED_EDGE ( 'NONE', *, *, #3528, .F. ) ;
#4819=PRODUCT_DEFINITION_SHAPE ( 'NONE', 'NONE',  #2684 ) ;
#4824=DIRECTION ( 'NONE',  ( -1.000000000000000000, -0.000000000000000000, -0.000000000000000000 ) ) ;
#4840=DIRECTION ( 'NONE',  ( 0.000000000000000000, 0.000000000000000000, -1.000000000000000000 ) ) ;
#4844=FILL_AREA_STYLE_COLOUR ( '', #4862 ) ;
#4853=DIRECTION ( 'NONE',  ( -1.000000000000000000, -0.000000000000000000, -0.000000000000000000 ) ) ;
#4862=COLOUR_RGB ( '', 0.31764706, 0.68627451, 0.89019608) ;
#4864=DIRECTION ( 'NONE',  ( -0.000000000000000000, 0.000000000000000000, 1.000000000000000000 ) ) ;
#4868=DIRECTION ( 'NONE',  ( 0.000000000000000000, 1.000000000000000000, -1.224646799147353207E-16 ) ) ;
#4905=VECTOR ( 'NONE', #2703, 1000.000000000000000 ) ;
#4914=DIRECTION ( 'NONE',  ( 1.000000000000000000, 0.000000000000000000, 0.000000000000000000 ) ) ;
#4915=CARTESIAN_POINT ( 'NONE',  ( 2.000000000000000000, 1.773042676681340968, -2.276824562219559311E-15 ) ) ;
#4921=EDGE_CURVE ( 'NONE', #675, #4685, #3832, .T. ) ;
#4938=PRODUCT_DEFINITION_CONTEXT ( 'detailed design', #4442, 'design' ) ;
#4942=CARTESIAN_POINT ( 'NONE',  ( 24.00000000000000000, 1.971681346627238735E-16, -1.610000000000000098 ) ) ;
#4944=EDGE_LOOP ( 'NONE', ( #1570, #2770, #2683, #2474 ) ) ;
#4945=STYLED_ITEM ( 'NONE', ( #1136 ), #1407 ) ;
#4949=PLANE ( 'NONE',  #2251 ) ;
#4952=DIRECTION ( 'NONE',  ( 0.000000000000000000, 0.000000000000000000, 1.000000000000000000 ) ) ;
#4956=ORIENTED_EDGE ( 'NONE', *, *, #3748, .F. ) ;
ENDSEC;
END-ISO-10303-21;
